ISO-10303-21;
HEADER;
/* Generated by software containing ST-Developer
 * from STEP Tools, Inc. (www.steptools.com) 
 */

FILE_DESCRIPTION(
/* description */ ('Turntable on roller ring'),
/* implementation_level */ '2;1');

FILE_NAME(
/* name */ 'Outer race retainer (1).step',
/* time_stamp */ '2026-10-28T03:23:59-07:00',
/* author */ (''),
/* organization */ (''),
/* preprocessor_version */ 'ST-DEVELOPER v20.2',
/* originating_system */ 'Autodesk Translation Framework v15.17.0.0',
/* authorisation */ '');

FILE_SCHEMA (('AUTOMOTIVE_DESIGN { 1 0 10303 214 3 1 1 }'));
ENDSEC;

DATA;
#10=MECHANICAL_DESIGN_GEOMETRIC_PRESENTATION_REPRESENTATION('',(#666),#16281);
#547=SHAPE_REPRESENTATION_RELATIONSHIP('SRR','None',#16568,#602);
#602=ADVANCED_BREP_SHAPE_REPRESENTATION('',(#734),#16262);
#666=STYLED_ITEM('',(#16932),#734);
#734=MANIFOLD_SOLID_BREP('Body1',#8411);
#961=FACE_BOUND('',#2376,.T.);
#962=FACE_BOUND('',#2378,.T.);
#1213=PLANE('',#9954);
#1214=PLANE('',#9955);
#1664=FACE_OUTER_BOUND('',#2373,.T.);
#1665=FACE_OUTER_BOUND('',#2374,.T.);
#1666=FACE_OUTER_BOUND('',#2375,.T.);
#1667=FACE_OUTER_BOUND('',#2377,.T.);
#2373=EDGE_LOOP('',(#7337,#7338,#7339,#7340));
#2374=EDGE_LOOP('',(#7341,#7342,#7343,#7344));
#2375=EDGE_LOOP('',(#7345));
#2376=EDGE_LOOP('',(#7346));
#2377=EDGE_LOOP('',(#7347));
#2378=EDGE_LOOP('',(#7348));
#2940=LINE('',#15384,#3423);
#2941=LINE('',#15390,#3424);
#3423=VECTOR('',#12467,1.1);
#3424=VECTOR('',#12474,1.5);
#3837=CIRCLE('',#9949,1.1);
#3838=CIRCLE('',#9950,1.1);
#3839=CIRCLE('',#9952,1.5);
#3840=CIRCLE('',#9953,1.5);
#4513=VERTEX_POINT('',#15381);
#4514=VERTEX_POINT('',#15383);
#4515=VERTEX_POINT('',#15387);
#4516=VERTEX_POINT('',#15389);
#5479=EDGE_CURVE('',#4513,#4513,#3837,.T.);
#5480=EDGE_CURVE('',#4513,#4514,#2940,.T.);
#5481=EDGE_CURVE('',#4514,#4514,#3838,.T.);
#5482=EDGE_CURVE('',#4515,#4515,#3839,.T.);
#5483=EDGE_CURVE('',#4515,#4516,#2941,.T.);
#5484=EDGE_CURVE('',#4516,#4516,#3840,.T.);
#7337=ORIENTED_EDGE('',*,*,#5479,.F.);
#7338=ORIENTED_EDGE('',*,*,#5480,.T.);
#7339=ORIENTED_EDGE('',*,*,#5481,.T.);
#7340=ORIENTED_EDGE('',*,*,#5480,.F.);
#7341=ORIENTED_EDGE('',*,*,#5482,.F.);
#7342=ORIENTED_EDGE('',*,*,#5483,.T.);
#7343=ORIENTED_EDGE('',*,*,#5484,.T.);
#7344=ORIENTED_EDGE('',*,*,#5483,.F.);
#7345=ORIENTED_EDGE('',*,*,#5482,.T.);
#7346=ORIENTED_EDGE('',*,*,#5479,.T.);
#7347=ORIENTED_EDGE('',*,*,#5484,.F.);
#7348=ORIENTED_EDGE('',*,*,#5481,.F.);
#7821=CYLINDRICAL_SURFACE('',#9948,1.1);
#7822=CYLINDRICAL_SURFACE('',#9951,1.5);
#8267=ADVANCED_FACE('',(#1664),#7821,.F.);
#8268=ADVANCED_FACE('',(#1665),#7822,.T.);
#8269=ADVANCED_FACE('',(#1666,#961),#1213,.T.);
#8270=ADVANCED_FACE('',(#1667,#962),#1214,.F.);
#8411=CLOSED_SHELL('',(#8267,#8268,#8269,#8270));
#9947=AXIS2_PLACEMENT_3D('',#15379,#12461,#12462);
#9948=AXIS2_PLACEMENT_3D('',#15380,#12463,#12464);
#9949=AXIS2_PLACEMENT_3D('',#15382,#12465,#12466);
#9950=AXIS2_PLACEMENT_3D('',#15385,#12468,#12469);
#9951=AXIS2_PLACEMENT_3D('',#15386,#12470,#12471);
#9952=AXIS2_PLACEMENT_3D('',#15388,#12472,#12473);
#9953=AXIS2_PLACEMENT_3D('',#15391,#12475,#12476);
#9954=AXIS2_PLACEMENT_3D('',#15392,#12477,#12478);
#9955=AXIS2_PLACEMENT_3D('',#15393,#12479,#12480);
#12461=DIRECTION('axis',(0.,0.,1.));
#12462=DIRECTION('refdir',(1.,0.,0.));
#12463=DIRECTION('center_axis',(0.,1.,0.));
#12464=DIRECTION('ref_axis',(1.,0.,0.));
#12465=DIRECTION('center_axis',(0.,-1.,0.));
#12466=DIRECTION('ref_axis',(1.,0.,0.));
#12467=DIRECTION('',(0.,-1.,0.));
#12468=DIRECTION('center_axis',(0.,-1.,0.));
#12469=DIRECTION('ref_axis',(1.,0.,0.));
#12470=DIRECTION('center_axis',(0.,1.,0.));
#12471=DIRECTION('ref_axis',(1.,0.,0.));
#12472=DIRECTION('center_axis',(0.,1.,0.));
#12473=DIRECTION('ref_axis',(1.,0.,0.));
#12474=DIRECTION('',(0.,-1.,0.));
#12475=DIRECTION('center_axis',(0.,1.,0.));
#12476=DIRECTION('ref_axis',(1.,0.,0.));
#12477=DIRECTION('center_axis',(0.,1.,0.));
#12478=DIRECTION('ref_axis',(1.,0.,0.));
#12479=DIRECTION('center_axis',(0.,1.,0.));
#12480=DIRECTION('ref_axis',(1.,0.,0.));
#15379=CARTESIAN_POINT('',(0.,0.,0.));
#15380=CARTESIAN_POINT('Origin',(0.,15.45,3.5));
#15381=CARTESIAN_POINT('',(-1.1,15.65,3.5));
#15382=CARTESIAN_POINT('Origin',(0.,15.65,3.5));
#15383=CARTESIAN_POINT('',(-1.1,15.45,3.5));
#15384=CARTESIAN_POINT('',(-1.1,15.45,3.5));
#15385=CARTESIAN_POINT('Origin',(0.,15.45,3.5));
#15386=CARTESIAN_POINT('Origin',(0.,15.45,3.5));
#15387=CARTESIAN_POINT('',(-1.5,15.65,3.5));
#15388=CARTESIAN_POINT('Origin',(0.,15.65,3.5));
#15389=CARTESIAN_POINT('',(-1.5,15.45,3.5));
#15390=CARTESIAN_POINT('',(-1.5,15.45,3.5));
#15391=CARTESIAN_POINT('Origin',(0.,15.45,3.5));
#15392=CARTESIAN_POINT('Origin',(0.,15.65,3.5));
#15393=CARTESIAN_POINT('Origin',(0.,15.45,3.5));
#16193=UNCERTAINTY_MEASURE_WITH_UNIT(LENGTH_MEASURE(0.001),#16282,
'DISTANCE_ACCURACY_VALUE',
'Maximum model space distance between geometric entities at asserted c
onnectivities');
#16212=UNCERTAINTY_MEASURE_WITH_UNIT(LENGTH_MEASURE(0.001),#16282,
'DISTANCE_ACCURACY_VALUE',
'Maximum model space distance between geometric entities at asserted c
onnectivities');
#16262=(
GEOMETRIC_REPRESENTATION_CONTEXT(3)
GLOBAL_UNCERTAINTY_ASSIGNED_CONTEXT((#16193))
GLOBAL_UNIT_ASSIGNED_CONTEXT((#16282,#16284,#16285))
REPRESENTATION_CONTEXT('','3D')
);
#16281=(
GEOMETRIC_REPRESENTATION_CONTEXT(3)
GLOBAL_UNCERTAINTY_ASSIGNED_CONTEXT((#16212))
GLOBAL_UNIT_ASSIGNED_CONTEXT((#16282,#16284,#16285))
REPRESENTATION_CONTEXT('','3D')
);
#16282=(
LENGTH_UNIT()
NAMED_UNIT(*)
SI_UNIT(.CENTI.,.METRE.)
);
#16284=(
NAMED_UNIT(*)
PLANE_ANGLE_UNIT()
SI_UNIT($,.RADIAN.)
);
#16285=(
NAMED_UNIT(*)
SI_UNIT($,.STERADIAN.)
SOLID_ANGLE_UNIT()
);
#16335=SHAPE_DEFINITION_REPRESENTATION(#16469,#16568);
#16469=PRODUCT_DEFINITION_SHAPE('',$,#16637);
#16568=SHAPE_REPRESENTATION('',(#9947),#16262);
#16587=PRODUCT_DEFINITION_CONTEXT('part definition',#16793,'design');
#16637=PRODUCT_DEFINITION('Outer race retainer (1)',
'Outer race retainer (1)',#16705,#16587);
#16705=PRODUCT_DEFINITION_FORMATION('',$,#16844);
#16793=APPLICATION_CONTEXT(
'Core Data for Automotive Mechanical Design Process');
#16794=PRODUCT_CONTEXT('part definition',#16793,'mechanical');
#16844=PRODUCT('Outer race retainer (1)','Outer race retainer (1)',
'Outer race retainer (1)',(#16794));
#16926=COLOUR_RGB('Grey',0.48,0.52,0.57);
#16927=FILL_AREA_STYLE_COLOUR('',#16926);
#16928=FILL_AREA_STYLE('',(#16927));
#16929=SURFACE_STYLE_FILL_AREA(#16928);
#16930=SURFACE_SIDE_STYLE('',(#16929));
#16931=SURFACE_STYLE_USAGE(.BOTH.,#16930);
#16932=PRESENTATION_STYLE_ASSIGNMENT((#16931));
ENDSEC;
END-ISO-10303-21;
